ISO-10303-21;
HEADER;
FILE_DESCRIPTION (('STEP AP214'),
    '1' );
FILE_NAME ('Screw 2.step',
    '2026-10-26T17:37:43',
    ( '' ),
    ( '' ),
    'SwSTEP 2.0',
    'SolidWorks 2024',
    '' );
FILE_SCHEMA (( 'AUTOMOTIVE_DESIGN' ));
ENDSEC;

DATA;
#3=EDGE_LOOP ( 'NONE', ( #5328, #3633, #22102, #2471 ) ) ;
#35=ORIENTED_EDGE ( 'NONE', *, *, #2844, .F. ) ;
#39=PLANE ( 'NONE',  #20096 ) ;
#57=AXIS2_PLACEMENT_3D ( 'NONE', #16806, #751, #19035 ) ;
#60=CARTESIAN_POINT ( 'NONE',  ( -12.31900000000000084, -3660.140000000000327, 2247.392000000000280 ) ) ;
#214=EDGE_CURVE ( 'NONE', #861, #2826, #5753, .T. ) ;
#261=ORIENTED_EDGE ( 'NONE', *, *, #15365, .F. ) ;
#289=CARTESIAN_POINT ( 'NONE',  ( -12.69999999999073204, -3658.702685254750122, 2244.902497835748818 ) ) ;
#294=DIRECTION ( 'NONE',  ( 0.000000000000000000, -1.000000000000000000, 0.000000000000000000 ) ) ;
#296=VECTOR ( 'NONE', #22031, 1000.000000000000000 ) ;
#301=EDGE_LOOP ( 'NONE', ( #2124, #6129, #13077, #7264 ) ) ;
#322=CARTESIAN_POINT ( 'NONE',  ( -12.69999999999997442, -3657.007659094873816, 2247.391999999781547 ) ) ;
#383=DIRECTION ( 'NONE',  ( -1.000000000000000000, 2.330758767201999921E-14, 2.356218894535000080E-14 ) ) ;
#398=FACE_OUTER_BOUND ( 'NONE', #16979, .T. ) ;
#411=DIRECTION ( 'NONE',  ( -2.356218894535439317E-14, 0.000000000000000000, -1.000000000000000000 ) ) ;
#416=ADVANCED_BREP_SHAPE_REPRESENTATION ( '', ( #13560, #5611 ), #2257 ) ;
#435=CARTESIAN_POINT ( 'NONE',  ( -12.69999999999999929, -3661.706170453011509, 2250.104686796980332 ) ) ;
#451=AXIS2_PLACEMENT_3D ( 'NONE', #16867, #16981, #7976 ) ;
#517=DIRECTION ( 'NONE',  ( -1.000000000000000000, 0.000000000000000000, 3.885294924357999613E-13 ) ) ;
#538=CARTESIAN_POINT ( 'NONE',  ( -6.730999999999999872, -3660.140000000000327, 2247.392000000000280 ) ) ;
#545=AXIS2_PLACEMENT_3D ( 'NONE', #4764, #11911, #21519 ) ;
#598=EDGE_LOOP ( 'NONE', ( #2863, #2197, #6752, #20467 ) ) ;
#647=ORIENTED_EDGE ( 'NONE', *, *, #17355, .T. ) ;
#676=LINE ( 'NONE', #22333, #5098 ) ;
#697=ADVANCED_FACE ( 'NONE', ( #2864 ), #13179, .T. ) ;
#705=EDGE_CURVE ( 'NONE', #12409, #21968, #18378, .T. ) ;
#751=DIRECTION ( 'NONE',  ( 0.000000000000000000, -0.8660254037817188832, 0.5000000000047110094 ) ) ;
#772=EDGE_LOOP ( 'NONE', ( #1178, #16136, #20200, #22962 ) ) ;
#776=EDGE_CURVE ( 'NONE', #11037, #16275, #8276, .T. ) ;
#807=ADVANCED_FACE ( 'NONE', ( #6629 ), #3773, .T. ) ;
#817=TOROIDAL_SURFACE ( 'NONE', #3822, 1.905000000000000027, 1.270000000000000018 ) ;
#849=DIRECTION ( 'NONE',  ( -1.000000000000000000, 2.318894227180000040E-14, 2.343004830739999973E-14 ) ) ;
#861=VERTEX_POINT ( 'NONE', #7315 ) ;
#952=VERTEX_POINT ( 'NONE', #7431 ) ;
#1031=ORIENTED_EDGE ( 'NONE', *, *, #1491, .F. ) ;
#1060=EDGE_LOOP ( 'NONE', ( #18493, #3265, #9177, #20346 ) ) ;
#1064=DIRECTION ( 'NONE',  ( -2.318894227180156550E-14, -1.000000000000000000, 0.000000000000000000 ) ) ;
#1102=EDGE_CURVE ( 'NONE', #19933, #2928, #6479, .T. ) ;
#1136=ORIENTED_EDGE ( 'NONE', *, *, #9565, .T. ) ;
#1155=ORIENTED_EDGE ( 'NONE', *, *, #14885, .F. ) ;
#1178=ORIENTED_EDGE ( 'NONE', *, *, #4955, .T. ) ;
#1179=ORIENTED_EDGE ( 'NONE', *, *, #15365, .T. ) ;
#1221=FACE_OUTER_BOUND ( 'NONE', #1060, .T. ) ;
#1245=DIRECTION ( 'NONE',  ( 1.000000000000000000, -2.330758767201999921E-14, -2.339144844575000061E-14 ) ) ;
#1276=( BOUNDED_CURVE ( )  B_SPLINE_CURVE ( 3, ( #21761, #18012, #11101, #435 ),
 .UNSPECIFIED., .F., .T. ) 
 B_SPLINE_CURVE_WITH_KNOTS ( ( 4, 4 ),
 ( -8.881784197001252323E-16, 1.570796326722519565 ),
 .UNSPECIFIED. ) 
 CURVE ( )  GEOMETRIC_REPRESENTATION_ITEM ( )  RATIONAL_B_SPLINE_CURVE ( ( 1.000000000000000000, 0.8047378541414241804, 0.8047378541414241804, 1.000000000000000000 ) ) 
 REPRESENTATION_ITEM ( '' )  );
#1326=ORIENTED_EDGE ( 'NONE', *, *, #6161, .T. ) ;
#1363=DIRECTION ( 'NONE',  ( -0.000000000000000000, 0.8660254037825932949, 0.5000000000031962211 ) ) ;
#1365=FACE_BOUND ( 'NONE', #4862, .T. ) ;
#1399=ADVANCED_FACE ( 'NONE', ( #3879 ), #20061, .T. ) ;
#1419=ORIENTED_EDGE ( 'NONE', *, *, #20266, .F. ) ;
#1468=ADVANCED_FACE ( 'NONE', ( #18515 ), #8312, .T. ) ;
#1491=EDGE_CURVE ( 'NONE', #21023, #8893, #19537, .T. ) ;
#1543=CARTESIAN_POINT ( 'NONE',  ( -12.70000000000011831, -3660.140000000000327, 2242.311999999999898 ) ) ;
#1615=DIRECTION ( 'NONE',  ( -2.318894227180156550E-14, -1.000000000000000000, 0.000000000000000000 ) ) ;
#1655=TOROIDAL_SURFACE ( 'NONE', #6961, 5.080000000000000071, 0.3810000000000000053 ) ;
#1698=ORIENTED_EDGE ( 'NONE', *, *, #13499, .F. ) ;
#1707=AXIS2_PLACEMENT_3D ( 'NONE', #16017, #14154, #13911 ) ;
#1719=CARTESIAN_POINT ( 'NONE',  ( 19.05000000000000071, -3660.140000000000327, 2247.392000000000280 ) ) ;
#1722=PLANE ( 'NONE',  #12133 ) ;
#1725=DIRECTION ( 'NONE',  ( -2.879814920640999944E-14, -1.000000000000000000, -1.559530541638999969E-12 ) ) ;
#1812=DIRECTION ( 'NONE',  ( -1.000000000000000000, 2.330758767201999921E-14, 2.343004830739999973E-14 ) ) ;
#1898=ORIENTED_EDGE ( 'NONE', *, *, #20590, .F. ) ;
#1935=EDGE_LOOP ( 'NONE', ( #6565, #20675, #8274, #261 ) ) ;
#1958=VERTEX_POINT ( 'NONE', #22340 ) ;
#1997=DIRECTION ( 'NONE',  ( 3.028227728875025183E-14, 0.5000000000049040771, 0.8660254037816071948 ) ) ;
#2057=DIRECTION ( 'NONE',  ( 0.000000000000000000, 1.000000000000000000, 0.000000000000000000 ) ) ;
#2075=CARTESIAN_POINT ( 'NONE',  ( -12.31900000000001505, -3658.793799999857129, 2249.723686796825405 ) ) ;
#2124=ORIENTED_EDGE ( 'NONE', *, *, #20266, .T. ) ;
#2193=DIRECTION ( 'NONE',  ( -2.334777064352623371E-14, -1.000000000000000000, 0.000000000000000000 ) ) ;
#2197=ORIENTED_EDGE ( 'NONE', *, *, #9722, .T. ) ;
#2242=DIRECTION ( 'NONE',  ( 0.000000000000000000, 0.5000000000005969669, -0.8660254037840939834 ) ) ;
#2257=( GEOMETRIC_REPRESENTATION_CONTEXT ( 3 ) GLOBAL_UNCERTAINTY_ASSIGNED_CONTEXT ( ( #16741 ) ) GLOBAL_UNIT_ASSIGNED_CONTEXT ( ( #21126, #3419, #23094 ) ) REPRESENTATION_CONTEXT ( 'NONE', 'WORKASPACE' ) );
#2305=LINE ( 'NONE', #5947, #9852 ) ;
#2323=DIRECTION ( 'NONE',  ( 0.000000000000000000, 1.206582004152999850E-12, -1.000000000000000000 ) ) ;
#2399=ORIENTED_EDGE ( 'NONE', *, *, #9722, .F. ) ;
#2426=DIRECTION ( 'NONE',  ( 0.000000000000000000, 1.000000000000000000, 0.000000000000000000 ) ) ;
#2431=VECTOR ( 'NONE', #5091, 1000.000000000000000 ) ;
#2447=FACE_OUTER_BOUND ( 'NONE', #301, .T. ) ;
#2463=CARTESIAN_POINT ( 'NONE',  ( -12.31899999999988005, -3660.140000000000327, 2252.472000000000207 ) ) ;
#2471=ORIENTED_EDGE ( 'NONE', *, *, #15609, .F. ) ;
#2475=ORIENTED_EDGE ( 'NONE', *, *, #5543, .F. ) ;
#2492=VERTEX_POINT ( 'NONE', #15964 ) ;
#2523=DIRECTION ( 'NONE',  ( 1.000000000000000000, 0.000000000000000000, 0.000000000000000000 ) ) ;
#2546=DIRECTION ( 'NONE',  ( -2.343004830739999973E-14, -1.784212334590129905E-30, -1.000000000000000000 ) ) ;
#2606=CARTESIAN_POINT ( 'NONE',  ( 0.000000000000000000, 0.000000000000000000, 0.000000000000000000 ) ) ;
#2637=ORIENTED_EDGE ( 'NONE', *, *, #12280, .F. ) ;
#2641=CARTESIAN_POINT ( 'NONE',  ( 19.05000000000000071, -3656.965000000000146, 2247.392000000000280 ) ) ;
#2642=CARTESIAN_POINT ( 'NONE',  ( -8.890000000017000303, -3658.793800000000374, 2249.723686796999573 ) ) ;
#2655=CARTESIAN_POINT ( 'NONE',  ( -6.349999999999999645, -3660.140000000000327, 2247.392000000000280 ) ) ;
#2796=ORIENTED_EDGE ( 'NONE', *, *, #8158, .T. ) ;
#2826=VERTEX_POINT ( 'NONE', #9728 ) ;
#2844=EDGE_CURVE ( 'NONE', #15557, #22556, #18987, .T. ) ;
#2863=ORIENTED_EDGE ( 'NONE', *, *, #22579, .T. ) ;
#2864=FACE_OUTER_BOUND ( 'NONE', #9948, .T. ) ;
#2928=VERTEX_POINT ( 'NONE', #9619 ) ;
#2968=ORIENTED_EDGE ( 'NONE', *, *, #17310, .F. ) ;
#2996=DIRECTION ( 'NONE',  ( 0.000000000000000000, -1.000000000000000000, 0.000000000000000000 ) ) ;
#3002=PRODUCT_DEFINITION_SHAPE ( 'NONE', 'NONE',  #12786 ) ;
#3099=CARTESIAN_POINT ( 'NONE',  ( -6.731000000000118888, -3660.140000000000327, 2242.311999999999898 ) ) ;
#3145=DIRECTION ( 'NONE',  ( -1.000000000000000000, 0.000000000000000000, 0.000000000000000000 ) ) ;
#3149=DIRECTION ( 'NONE',  ( -1.159746789738050283E-14, -0.5000000000005221379, 0.8660254037841371710 ) ) ;
#3217=CARTESIAN_POINT ( 'NONE',  ( -8.890000000032001637, -3658.793800000000374, 2245.060313203000078 ) ) ;
#3226=DIRECTION ( 'NONE',  ( 0.000000000000000000, -1.000000000000000000, 0.000000000000000000 ) ) ;
#3263=PLANE ( 'NONE',  #17405 ) ;
#3265=ORIENTED_EDGE ( 'NONE', *, *, #15360, .T. ) ;
#3408=CARTESIAN_POINT ( 'NONE',  ( -12.31900000000000084, -3660.140000000000327, 2247.392000000000280 ) ) ;
#3412=ORIENTED_EDGE ( 'NONE', *, *, #14392, .F. ) ;
#3419=( NAMED_UNIT ( * ) PLANE_ANGLE_UNIT ( ) SI_UNIT ( $, .RADIAN. ) );
#3444=CARTESIAN_POINT ( 'NONE',  ( -6.730999999999872863, -3660.140000000000327, 2252.853000000000065 ) ) ;
#3448=CARTESIAN_POINT ( 'NONE',  ( -6.349999999999999645, -3660.140000000000327, 2247.392000000000280 ) ) ;
#3451=ORIENTED_EDGE ( 'NONE', *, *, #6945, .F. ) ;
#3463=AXIS2_PLACEMENT_3D ( 'NONE', #9873, #13279, #18444 ) ;
#3489=CLOSED_SHELL ( 'NONE', ( #15133, #15720, #807, #10568, #14427, #9706, #6724, #8142, #12688, #11075, #12372, #1399, #697, #20814, #10739, #8144, #11809, #12080, #21605, #11371, #23130, #1468, #22244, #13702, #17948, #11438 ) ) ;
#3555=DIRECTION ( 'NONE',  ( 1.000000000000000000, -2.334777064353000131E-14, -2.343004830739999973E-14 ) ) ;
#3567=DIRECTION ( 'NONE',  ( 0.000000000000000000, -1.000000000000000000, -2.848874176402999842E-12 ) ) ;
#3577=VECTOR ( 'NONE', #13440, 1000.000000000000227 ) ;
#3597=AXIS2_PLACEMENT_3D ( 'NONE', #21374, #11174, #18313 ) ;
#3628=VECTOR ( 'NONE', #14541, 1000.000000000000000 ) ;
#3633=ORIENTED_EDGE ( 'NONE', *, *, #12507, .F. ) ;
#3641=CYLINDRICAL_SURFACE ( 'NONE', #21140, 0.3809999999999121312 ) ;
#3666=CIRCLE ( 'NONE', #11170, 5.460999999999938126 ) ;
#3723=ORIENTED_EDGE ( 'NONE', *, *, #4779, .T. ) ;
#3769=CYLINDRICAL_SURFACE ( 'NONE', #21280, 0.3809999999999647002 ) ;
#3773=TOROIDAL_SURFACE ( 'NONE', #13144, 5.080000000000000071, 0.3810000000000000053 ) ;
#3793=DIRECTION ( 'NONE',  ( -1.417468298637000021E-14, -1.000000000000000000, -1.484475890936000021E-12 ) ) ;
#3804=EDGE_LOOP ( 'NONE', ( #9544, #2399, #15395, #2968 ) ) ;
#3822=AXIS2_PLACEMENT_3D ( 'NONE', #15328, #6086, #9594 ) ;
#3847=DIRECTION ( 'NONE',  ( -1.000000000000000000, 0.000000000000000000, 0.000000000000000000 ) ) ;
#3879=FACE_OUTER_BOUND ( 'NONE', #21281, .T. ) ;
#3880=DIRECTION ( 'NONE',  ( 0.000000000000000000, -1.000000000000000000, 0.000000000000000000 ) ) ;
#3909=CARTESIAN_POINT ( 'NONE',  ( -12.31900000000000084, -3658.793799999878502, 2245.060313203211081 ) ) ;
#3917=CARTESIAN_POINT ( 'NONE',  ( -12.69999999986624495, -3658.702685254810149, 2249.881502164143058 ) ) ;
#3931=ORIENTED_EDGE ( 'NONE', *, *, #705, .T. ) ;
#3991=VERTEX_POINT ( 'NONE', #17335 ) ;
#3999=CARTESIAN_POINT ( 'NONE',  ( -8.890000000024000926, -3657.447599999999966, 2247.392000000000280 ) ) ;
#4030=ORIENTED_EDGE ( 'NONE', *, *, #7433, .T. ) ;
#4066=CARTESIAN_POINT ( 'NONE',  ( -8.890000000026999416, -3657.447599999999966, 2247.392000000000280 ) ) ;
#4070=EDGE_CURVE ( 'NONE', #2928, #15033, #4692, .T. ) ;
#4076=APPLICATION_CONTEXT ( 'configuration controlled 3d designs of mechanical parts and assemblies' ) ;
#4110=CARTESIAN_POINT ( 'NONE',  ( -6.730999999999999872, -3660.140000000000327, 2247.392000000000280 ) ) ;
#4139=CARTESIAN_POINT ( 'NONE',  ( -6.730999999999999872, -3660.140000000000327, 2247.392000000000280 ) ) ;
#4182=ORIENTED_EDGE ( 'NONE', *, *, #9547, .T. ) ;
#4255=TOROIDAL_SURFACE ( 'NONE', #4612, 1.905000000000000027, 1.270000000000000018 ) ;
#4271=CARTESIAN_POINT ( 'NONE',  ( -6.349999999999999645, -3663.315000000000509, 2247.392000000000280 ) ) ;
#4397=DIRECTION ( 'NONE',  ( -2.330758767202000237E-14, -1.000000000000000000, -1.224646799141892318E-16 ) ) ;
#4492=VECTOR ( 'NONE', #12977, 999.9999999999998863 ) ;
#4499=ORIENTED_EDGE ( 'NONE', *, *, #13499, .T. ) ;
#4524=EDGE_LOOP ( 'NONE', ( #21514, #20558, #5691, #9992 ) ) ;
#4527=CARTESIAN_POINT ( 'NONE',  ( -12.31900000000000084, -3661.486200000121244, 2249.723686796789480 ) ) ;
#4535=AXIS2_PLACEMENT_3D ( 'NONE', #10251, #20680, #3226 ) ;
#4581=AXIS2_PLACEMENT_3D ( 'NONE', #21935, #383, #5901 ) ;
#4612=AXIS2_PLACEMENT_3D ( 'NONE', #19323, #12833, #2057 ) ;
#4683=VECTOR ( 'NONE', #3149, 1000.000000000000227 ) ;
#4692=LINE ( 'NONE', #8333, #10379 ) ;
#4710=DIRECTION ( 'NONE',  ( -3.322863369922961486E-14, -0.5000000000038942183, -0.8660254037821902839 ) ) ;
#4764=CARTESIAN_POINT ( 'NONE',  ( 20.32000000000000028, -3660.140000000000327, 2247.392000000000280 ) ) ;
#4770=EDGE_CURVE ( 'NONE', #13205, #22556, #10988, .T. ) ;
#4779=EDGE_CURVE ( 'NONE', #2492, #8893, #7883, .T. ) ;
#4784=CARTESIAN_POINT ( 'NONE',  ( -12.31899999999987294, -3654.679000000000087, 2247.392000000000280 ) ) ;
#4812=ORIENTED_EDGE ( 'NONE', *, *, #22824, .F. ) ;
#4853=ORIENTED_EDGE ( 'NONE', *, *, #12280, .T. ) ;
#4862=EDGE_LOOP ( 'NONE', ( #18399, #12578, #4030, #1155, #21148, #8173 ) ) ;
#4867=DIRECTION ( 'NONE',  ( 3.410299865766000309E-12, -1.000000000000000000, -9.896505939573000930E-13 ) ) ;
#4929=VECTOR ( 'NONE', #4710, 1000.000000000000000 ) ;
#4955=EDGE_CURVE ( 'NONE', #20085, #10748, #11904, .T. ) ;
#4965=EDGE_CURVE ( 'NONE', #8583, #16226, #20928, .T. ) ;
#4979=VECTOR ( 'NONE', #3793, 1000.000000000000000 ) ;
#4980=DIRECTION ( 'NONE',  ( 0.000000000000000000, -1.165588477296860248E-12, 1.000000000000000000 ) ) ;
#5091=DIRECTION ( 'NONE',  ( -1.000000000000000000, 0.000000000000000000, 2.590196616235000036E-13 ) ) ;
#5098=VECTOR ( 'NONE', #22443, 1000.000000000000114 ) ;
#5103=CYLINDRICAL_SURFACE ( 'NONE', #20951, 5.460999999999938126 ) ;
#5106=ORIENTED_EDGE ( 'NONE', *, *, #10879, .F. ) ;
#5271=EDGE_CURVE ( 'NONE', #16784, #12197, #18781, .T. ) ;
#5277=APPLICATION_CONTEXT ( 'configuration controlled 3d designs of mechanical parts and assemblies' ) ;
#5328=ORIENTED_EDGE ( 'NONE', *, *, #12801, .F. ) ;
#5380=ORIENTED_EDGE ( 'NONE', *, *, #8124, .T. ) ;
#5389=FACE_OUTER_BOUND ( 'NONE', #6047, .T. ) ;
#5400=LINE ( 'NONE', #14542, #21601 ) ;
#5410=DIRECTION ( 'NONE',  ( 0.000000000000000000, -0.8660254037817070039, 0.5000000000047313264 ) ) ;
#5542=DIRECTION ( 'NONE',  ( 0.000000000000000000, 1.000000000000000000, 0.000000000000000000 ) ) ;
#5543=EDGE_CURVE ( 'NONE', #15415, #7536, #5400, .T. ) ;
#5611=AXIS2_PLACEMENT_3D ( 'NONE', #2606, #9751, #7545 ) ;
#5620=CARTESIAN_POINT ( 'NONE',  ( 19.05000000000000071, -3658.235000000000127, 2247.392000000000280 ) ) ;
#5645=CARTESIAN_POINT ( 'NONE',  ( -12.31900000000000084, -3661.486200000000281, 2245.060313203000078 ) ) ;
#5688=CARTESIAN_POINT ( 'NONE',  ( -6.731000000000127770, -3665.601000000000113, 2247.392000000000280 ) ) ;
#5691=ORIENTED_EDGE ( 'NONE', *, *, #20167, .F. ) ;
#5694=CARTESIAN_POINT ( 'NONE',  ( -12.69999999999999929, -3660.140000000000327, 2247.392000000000280 ) ) ;
#5722=CARTESIAN_POINT ( 'NONE',  ( -12.31899999999994755, -3657.447599999831709, 2247.391999999993914 ) ) ;
#5753=CIRCLE ( 'NONE', #9123, 5.460999999999938126 ) ;
#5760=VECTOR ( 'NONE', #21739, 1000.000000000000000 ) ;
#5764=ORIENTED_EDGE ( 'NONE', *, *, #10063, .T. ) ;
#5817=ORIENTED_EDGE ( 'NONE', *, *, #776, .T. ) ;
#5844=DIRECTION ( 'NONE',  ( 1.000000000000000000, 0.000000000000000000, 0.000000000000000000 ) ) ;
#5881=ORIENTED_EDGE ( 'NONE', *, *, #4965, .T. ) ;
#5901=DIRECTION ( 'NONE',  ( -2.356218894535439317E-14, 0.000000000000000000, -1.000000000000000000 ) ) ;
#5947=CARTESIAN_POINT ( 'NONE',  ( -6.349999999999999645, -3665.601000000000113, 2247.392000000000280 ) ) ;
#6001=CARTESIAN_POINT ( 'NONE',  ( 20.32000000000000028, -3662.045000000000073, 2247.392000000000280 ) ) ;
#6047=EDGE_LOOP ( 'NONE', ( #20542, #18726 ) ) ;
#6062=LINE ( 'NONE', #20348, #15773 ) ;
#6081=CARTESIAN_POINT ( 'NONE',  ( -6.730999999999999872, -3660.140000000000327, 2247.392000000000280 ) ) ;
#6086=DIRECTION ( 'NONE',  ( 1.000000000000000000, 0.000000000000000000, 0.000000000000000000 ) ) ;
#6129=ORIENTED_EDGE ( 'NONE', *, *, #1491, .T. ) ;
#6135=ORIENTED_EDGE ( 'NONE', *, *, #11116, .T. ) ;
#6138=CIRCLE ( 'NONE', #17337, 5.079999999999973426 ) ;
#6157=ORIENTED_EDGE ( 'NONE', *, *, #18020, .T. ) ;
#6161=EDGE_CURVE ( 'NONE', #12197, #6431, #18942, .T. ) ;
#6176=DIRECTION ( 'NONE',  ( -3.028227728787145447E-14, -0.5000000000043240966, -0.8660254037819421491 ) ) ;
#6186=FACE_OUTER_BOUND ( 'NONE', #16742, .T. ) ;
#6218=DIRECTION ( 'NONE',  ( 0.000000000000000000, -0.8660254037825031448, -0.5000000000033524294 ) ) ;
#6245=DIRECTION ( 'NONE',  ( 0.000000000000000000, 1.000000000000000000, 0.000000000000000000 ) ) ;
#6286=CARTESIAN_POINT ( 'NONE',  ( -8.890000000008001280, -3661.486200000000281, 2249.723686796999573 ) ) ;
#6318=CARTESIAN_POINT ( 'NONE',  ( -12.70000000000007923, -3661.706170452909191, 2244.679313203225774 ) ) ;
#6338=DIRECTION ( 'NONE',  ( -2.343004830739999973E-14, -1.784212334590129905E-30, -1.000000000000000000 ) ) ;
#6362=CARTESIAN_POINT ( 'NONE',  ( -12.31900000000012874, -3660.140000000000327, 2241.931000000000040 ) ) ;
#6431=VERTEX_POINT ( 'NONE', #4271 ) ;
#6479=LINE ( 'NONE', #20763, #4929 ) ;
#6481=ORIENTED_EDGE ( 'NONE', *, *, #17985, .T. ) ;
#6523=AXIS2_PLACEMENT_3D ( 'NONE', #6748, #12009, #4980 ) ;
#6562=ORIENTED_EDGE ( 'NONE', *, *, #22824, .T. ) ;
#6565=ORIENTED_EDGE ( 'NONE', *, *, #21463, .F. ) ;
#6617=CARTESIAN_POINT ( 'NONE',  ( -8.890000000017000303, -3658.793800000000374, 2249.723686796999573 ) ) ;
#6629=FACE_OUTER_BOUND ( 'NONE', #16451, .T. ) ;
#6638=CYLINDRICAL_SURFACE ( 'NONE', #6523, 0.3809999999999647002 ) ;
#6658=VERTEX_POINT ( 'NONE', #16797 ) ;
#6724=ADVANCED_FACE ( 'NONE', ( #6965 ), #39, .F. ) ;
#6748=CARTESIAN_POINT ( 'NONE',  ( -12.31900000000000084, -3660.140000000000327, 2250.104686796999886 ) ) ;
#6752=ORIENTED_EDGE ( 'NONE', *, *, #11854, .T. ) ;
#6770=FACE_OUTER_BOUND ( 'NONE', #3, .T. ) ;
#6782=AXIS2_PLACEMENT_3D ( 'NONE', #22652, #3555, #14232 ) ;
#6831=ORIENTED_EDGE ( 'NONE', *, *, #705, .F. ) ;
#6857=DIRECTION ( 'NONE',  ( -2.343004830739999973E-14, -1.784212334590129905E-30, -1.000000000000000000 ) ) ;
#6941=AXIS2_PLACEMENT_3D ( 'NONE', #5620, #21666, #12644 ) ;
#6945=EDGE_CURVE ( 'NONE', #21023, #16784, #17408, .T. ) ;
#6961=AXIS2_PLACEMENT_3D ( 'NONE', #22332, #16944, #2546 ) ;
#6963=AXIS2_PLACEMENT_3D ( 'NONE', #22267, #7878, #6245 ) ;
#6965=FACE_OUTER_BOUND ( 'NONE', #8081, .T. ) ;
#7009=DIRECTION ( 'NONE',  ( 1.000000000000000000, 0.000000000000000000, 0.000000000000000000 ) ) ;
#7010=PLANE ( 'NONE',  #1707 ) ;
#7065=DIRECTION ( 'NONE',  ( -1.000000000000000000, 0.000000000000000000, 0.000000000000000000 ) ) ;
#7078=AXIS2_PLACEMENT_3D ( 'NONE', #16163, #21893, #14756 ) ;
#7100=CARTESIAN_POINT ( 'NONE',  ( -12.69999999999998153, -3658.573829547082369, 2250.104686796773422 ) ) ;
#7144=PLANE ( 'NONE',  #7078 ) ;
#7191=ORIENTED_EDGE ( 'NONE', *, *, #7433, .F. ) ;
#7264=ORIENTED_EDGE ( 'NONE', *, *, #12299, .F. ) ;
#7268=CARTESIAN_POINT ( 'NONE',  ( -8.890000000022000748, -3661.486200000000281, 2245.060313203000078 ) ) ;
#7302=DIRECTION ( 'NONE',  ( -1.000000000000000000, 0.000000000000000000, 0.000000000000000000 ) ) ;
#7315=CARTESIAN_POINT ( 'NONE',  ( -12.31900000000012696, -3665.601000000000113, 2247.392000000000280 ) ) ;
#7320=DIRECTION ( 'NONE',  ( -1.000000000000000000, 0.000000000000000000, 0.000000000000000000 ) ) ;
#7329=AXIS2_PLACEMENT_3D ( 'NONE', #10530, #22821, #1615 ) ;
#7345=LINE ( 'NONE', #21524, #8022 ) ;
#7387=LINE ( 'NONE', #7268, #3628 ) ;
#7400=DIRECTION ( 'NONE',  ( 4.316835273014999614E-14, 1.000000000000000000, 2.309184719176999840E-12 ) ) ;
#7431=CARTESIAN_POINT ( 'NONE',  ( -8.890000000008999592, -3662.832400000000234, 2247.392000000000280 ) ) ;
#7433=EDGE_CURVE ( 'NONE', #1958, #3991, #15495, .T. ) ;
#7476=VERTEX_POINT ( 'NONE', #1543 ) ;
#7511=CARTESIAN_POINT ( 'NONE',  ( 20.32000000000000028, -3660.140000000000327, 2247.392000000000280 ) ) ;
#7536=VERTEX_POINT ( 'NONE', #8353 ) ;
#7545=DIRECTION ( 'NONE',  ( 1.000000000000000000, 0.000000000000000000, 0.000000000000000000 ) ) ;
#7714=ORIENTED_EDGE ( 'NONE', *, *, #9565, .F. ) ;
#7748=EDGE_LOOP ( 'NONE', ( #1419, #22998, #11862, #19788 ) ) ;
#7775=EDGE_LOOP ( 'NONE', ( #647, #6157 ) ) ;
#7848=EDGE_CURVE ( 'NONE', #8227, #861, #2305, .T. ) ;
#7878=DIRECTION ( 'NONE',  ( 1.000000000000000000, 0.000000000000000000, 0.000000000000000000 ) ) ;
#7883=CIRCLE ( 'NONE', #20983, 1.904999999999823501 ) ;
#7949=EDGE_CURVE ( 'NONE', #22852, #12409, #20718, .T. ) ;
#7950=ORIENTED_EDGE ( 'NONE', *, *, #776, .F. ) ;
#7972=CIRCLE ( 'NONE', #3463, 0.3809999999999993947 ) ;
#7973=ORIENTED_EDGE ( 'NONE', *, *, #17102, .T. ) ;
#7976=DIRECTION ( 'NONE',  ( 0.000000000000000000, -1.000000000000000000, 0.000000000000000000 ) ) ;
#8022=VECTOR ( 'NONE', #9220, 1000.000000000000227 ) ;
#8081=EDGE_LOOP ( 'NONE', ( #5764, #22807, #8611, #21806, #20785, #35 ) ) ;
#8086=CIRCLE ( 'NONE', #14818, 3.175000000000149925 ) ;
#8124=EDGE_CURVE ( 'NONE', #22852, #11037, #19699, .T. ) ;
#8142=ADVANCED_FACE ( 'NONE', ( #22777 ), #8850, .T. ) ;
#8144=ADVANCED_FACE ( 'NONE', ( #1221 ), #6638, .T. ) ;
#8158=EDGE_CURVE ( 'NONE', #22556, #15415, #19161, .T. ) ;
#8173=ORIENTED_EDGE ( 'NONE', *, *, #4070, .T. ) ;
#8227=VERTEX_POINT ( 'NONE', #5688 ) ;
#8274=ORIENTED_EDGE ( 'NONE', *, *, #5543, .T. ) ;
#8276=CIRCLE ( 'NONE', #6782, 5.460999999999938126 ) ;
#8312=TOROIDAL_SURFACE ( 'NONE', #18413, 5.080000000000000071, 0.3810000000000000053 ) ;
#8333=CARTESIAN_POINT ( 'NONE',  ( -12.69999999999999929, -3663.272340904999965, 2247.392000000000280 ) ) ;
#8353=CARTESIAN_POINT ( 'NONE',  ( -12.31899999999994755, -3657.447599999831709, 2247.391999999993914 ) ) ;
#8377=EDGE_LOOP ( 'NONE', ( #3723, #12643 ) ) ;
#8394=ORIENTED_EDGE ( 'NONE', *, *, #8124, .F. ) ;
#8458=AXIS2_PLACEMENT_3D ( 'NONE', #2655, #1245, #13207 ) ;
#8484=( BOUNDED_CURVE ( )  B_SPLINE_CURVE ( 3, ( #18645, #13375, #16657, #20516 ),
 .UNSPECIFIED., .F., .F. ) 
 B_SPLINE_CURVE_WITH_KNOTS ( ( 4, 4 ),
 ( 4.620504083482610562E-16, 1.570796326138795385 ),
 .UNSPECIFIED. ) 
 CURVE ( )  GEOMETRIC_REPRESENTATION_ITEM ( )  RATIONAL_B_SPLINE_CURVE ( ( 1.000000000000000000, 0.8047378542790095679, 0.8047378542790095679, 1.000000000000000000 ) ) 
 REPRESENTATION_ITEM ( '' )  );
#8528=FACE_OUTER_BOUND ( 'NONE', #7775, .T. ) ;
#8536=VECTOR ( 'NONE', #17141, 1000.000000000000000 ) ;
#8575=ORIENTED_EDGE ( 'NONE', *, *, #9547, .F. ) ;
#8583=VERTEX_POINT ( 'NONE', #17356 ) ;
#8601=LINE ( 'NONE', #22649, #2431 ) ;
#8611=ORIENTED_EDGE ( 'NONE', *, *, #4965, .F. ) ;
#8631=DIRECTION ( 'NONE',  ( 0.000000000000000000, 1.000000000000000000, 0.000000000000000000 ) ) ;
#8837=AXIS2_PLACEMENT_3D ( 'NONE', #3099, #21275, #14129 ) ;
#8850=PLANE ( 'NONE',  #17730 ) ;
#8893=VERTEX_POINT ( 'NONE', #6001 ) ;
#8925=CARTESIAN_POINT ( 'NONE',  ( 19.05000000000000071, -3660.140000000000327, 2247.392000000000280 ) ) ;
#8968=CARTESIAN_POINT ( 'NONE',  ( -12.31900000000001505, -3658.793799999857129, 2249.723686796825405 ) ) ;
#9015=FACE_BOUND ( 'NONE', #17374, .T. ) ;
#9053=CARTESIAN_POINT ( 'NONE',  ( -12.31900000000000084, -3660.140000000000327, 2244.679313203000220 ) ) ;
#9065=CYLINDRICAL_SURFACE ( 'NONE', #3597, 0.3809999999999121312 ) ;
#9121=AXIS2_PLACEMENT_3D ( 'NONE', #60, #1812, #21504 ) ;
#9123=AXIS2_PLACEMENT_3D ( 'NONE', #3408, #10562, #1064 ) ;
#9176=LINE ( 'NONE', #16321, #18437 ) ;
#9177=ORIENTED_EDGE ( 'NONE', *, *, #14885, .T. ) ;
#9193=CARTESIAN_POINT ( 'NONE',  ( -6.349999999999999645, -3660.140000000000327, 2247.392000000000280 ) ) ;
#9220=DIRECTION ( 'NONE',  ( -1.804050561861959928E-14, 0.5000000000033889558, -0.8660254037824819395 ) ) ;
#9405=CARTESIAN_POINT ( 'NONE',  ( -6.730999999999872863, -3654.679000000000087, 2247.392000000000280 ) ) ;
#9438=EDGE_CURVE ( 'NONE', #8583, #13205, #20129, .T. ) ;
#9494=LINE ( 'NONE', #5645, #15507 ) ;
#9517=ORIENTED_EDGE ( 'NONE', *, *, #7949, .F. ) ;
#9544=ORIENTED_EDGE ( 'NONE', *, *, #12801, .T. ) ;
#9547=EDGE_CURVE ( 'NONE', #16505, #20980, #3666, .T. ) ;
#9550=ORIENTED_EDGE ( 'NONE', *, *, #10879, .T. ) ;
#9565=EDGE_CURVE ( 'NONE', #8583, #22551, #12454, .T. ) ;
#9592=ORIENTED_EDGE ( 'NONE', *, *, #15296, .T. ) ;
#9594=DIRECTION ( 'NONE',  ( 0.000000000000000000, 1.000000000000000000, 0.000000000000000000 ) ) ;
#9619=CARTESIAN_POINT ( 'NONE',  ( -12.70000000000005080, -3663.272340905245528, 2247.392000000001644 ) ) ;
#9697=ORIENTED_EDGE ( 'NONE', *, *, #11116, .F. ) ;
#9702=VECTOR ( 'NONE', #16812, 1000.000000000000000 ) ;
#9706=ADVANCED_FACE ( 'NONE', ( #12799 ), #3769, .T. ) ;
#9722=EDGE_CURVE ( 'NONE', #15033, #16863, #23108, .T. ) ;
#9728=CARTESIAN_POINT ( 'NONE',  ( -12.31899999999987116, -3660.140000000000327, 2252.853000000000065 ) ) ;
#9751=DIRECTION ( 'NONE',  ( 0.000000000000000000, 0.000000000000000000, 1.000000000000000000 ) ) ;
#9809=AXIS2_PLACEMENT_3D ( 'NONE', #11645, #10019, #13187 ) ;
#9836=DIRECTION ( 'NONE',  ( -1.000000000000000000, 2.330758767201999921E-14, 2.343004830739999973E-14 ) ) ;
#9852=VECTOR ( 'NONE', #21870, 1000.000000000000000 ) ;
#9873=CARTESIAN_POINT ( 'NONE',  ( -12.31900000000011985, -3660.140000000000327, 2242.311999999999898 ) ) ;
#9911=AXIS2_PLACEMENT_3D ( 'NONE', #8925, #7065, #3880 ) ;
#9948=EDGE_LOOP ( 'NONE', ( #2475, #19379, #12958, #16941 ) ) ;
#9992=ORIENTED_EDGE ( 'NONE', *, *, #12507, .T. ) ;
#10019=DIRECTION ( 'NONE',  ( 1.000000000000000000, -2.330758767201999921E-14, -2.339144844575000061E-14 ) ) ;
#10063=EDGE_CURVE ( 'NONE', #15557, #952, #7387, .T. ) ;
#10138=PRODUCT_DEFINITION_FORMATION_WITH_SPECIFIED_SOURCE ( 'ANY', '', #21176, .NOT_KNOWN. ) ;
#10233=ORIENTED_EDGE ( 'NONE', *, *, #5271, .F. ) ;
#10251=CARTESIAN_POINT ( 'NONE',  ( 19.05000000000000071, -3660.140000000000327, 2247.392000000000280 ) ) ;
#10296=CARTESIAN_POINT ( 'NONE',  ( -12.69999999999999929, -3661.706170453011509, 2250.104686796980332 ) ) ;
#10366=DIRECTION ( 'NONE',  ( 0.000000000000000000, -1.000000000000000000, 0.000000000000000000 ) ) ;
#10379=VECTOR ( 'NONE', #15477, 1000.000000000000114 ) ;
#10452=DIRECTION ( 'NONE',  ( 0.000000000000000000, -0.5000000000006717960, 0.8660254037840506847 ) ) ;
#10506=LINE ( 'NONE', #16132, #23157 ) ;
#10515=DIRECTION ( 'NONE',  ( -2.318894227180156550E-14, -1.000000000000000000, 0.000000000000000000 ) ) ;
#10530=CARTESIAN_POINT ( 'NONE',  ( -12.31900000000000084, -3660.140000000000327, 2247.392000000000280 ) ) ;
#10541=ORIENTED_EDGE ( 'NONE', *, *, #9438, .F. ) ;
#10562=DIRECTION ( 'NONE',  ( -1.000000000000000000, 2.318894227180000040E-14, 2.343004830739999973E-14 ) ) ;
#10568=ADVANCED_FACE ( 'NONE', ( #20916 ), #12005, .T. ) ;
#10575=SHAPE_REPRESENTATION_RELATIONSHIP ( 'NONE' , 'NONE' ,  #15665, #416 ) ;
#10677=AXIS2_PLACEMENT_3D ( 'NONE', #11223, #2323, #3847 ) ;
#10717=CARTESIAN_POINT ( 'NONE',  ( -12.31900000000000084, -3657.790744320999693, 2248.748343399000532 ) ) ;
#10727=CARTESIAN_POINT ( 'NONE',  ( -12.31900000000002393, -3661.486200000138069, 2245.060313203176065 ) ) ;
#10739=ADVANCED_FACE ( 'NONE', ( #398 ), #14699, .T. ) ;
#10748=VERTEX_POINT ( 'NONE', #21843 ) ;
#10879=EDGE_CURVE ( 'NONE', #2826, #15463, #14473, .T. ) ;
#10883=CARTESIAN_POINT ( 'NONE',  ( -6.349999999999880629, -3660.140000000000327, 2252.472000000000207 ) ) ;
#10988=LINE ( 'NONE', #4066, #4492 ) ;
#11027=DIRECTION ( 'NONE',  ( 1.000000000000000000, 0.000000000000000000, 0.000000000000000000 ) ) ;
#11037=VERTEX_POINT ( 'NONE', #19086 ) ;
#11047=CIRCLE ( 'NONE', #6941, 1.270000000000000240 ) ;
#11075=ADVANCED_FACE ( 'NONE', ( #19208 ), #3263, .T. ) ;
#11101=CARTESIAN_POINT ( 'NONE',  ( -12.69999999998383977, -3661.577314745246440, 2249.881502164247649 ) ) ;
#11116=EDGE_CURVE ( 'NONE', #20980, #861, #22268, .T. ) ;
#11163=CARTESIAN_POINT ( 'NONE',  ( -12.69999999986526795, -3661.577314745183230, 2244.902497835854774 ) ) ;
#11170=AXIS2_PLACEMENT_3D ( 'NONE', #14624, #849, #13399 ) ;
#11174=DIRECTION ( 'NONE',  ( 3.194481088216070180E-14, 0.5000000000047110094, 0.8660254037817188832 ) ) ;
#11196=EDGE_LOOP ( 'NONE', ( #10233, #3451, #6481, #19380 ) ) ;
#11223=CARTESIAN_POINT ( 'NONE',  ( -8.890000000018000392, -3658.793800000000374, 2249.723686796999573 ) ) ;
#11323=CIRCLE ( 'NONE', #4581, 5.079999999999973426 ) ;
#11343=ORIENTED_EDGE ( 'NONE', *, *, #214, .T. ) ;
#11371=ADVANCED_FACE ( 'NONE', ( #6186 ), #1655, .T. ) ;
#11423=LINE ( 'NONE', #6286, #9702 ) ;
#11431=DIRECTION ( 'NONE',  ( 1.000000000000000000, -2.590196616232000093E-13, 0.000000000000000000 ) ) ;
#11438=ADVANCED_FACE ( 'NONE', ( #13670 ), #20820, .F. ) ;
#11637=CARTESIAN_POINT ( 'NONE',  ( -6.730999999999880856, -3660.140000000000327, 2252.472000000000207 ) ) ;
#11645=CARTESIAN_POINT ( 'NONE',  ( -6.349999999999999645, -3660.140000000000327, 2247.392000000000280 ) ) ;
#11715=ORIENTED_EDGE ( 'NONE', *, *, #22391, .F. ) ;
#11809=ADVANCED_FACE ( 'NONE', ( #22530 ), #3641, .T. ) ;
#11819=DIRECTION ( 'NONE',  ( 1.000000000000000000, 0.000000000000000000, 0.000000000000000000 ) ) ;
#11824=CYLINDRICAL_SURFACE ( 'NONE', #18519, 0.3810000000000746678 ) ;
#11831=PRODUCT_DEFINITION_CONTEXT ( 'detailed design', #5277, 'design' ) ;
#11854=EDGE_CURVE ( 'NONE', #16863, #15415, #9494, .T. ) ;
#11862=ORIENTED_EDGE ( 'NONE', *, *, #14260, .F. ) ;
#11904=LINE ( 'NONE', #13312, #22412 ) ;
#11911=DIRECTION ( 'NONE',  ( -1.000000000000000000, 0.000000000000000000, 0.000000000000000000 ) ) ;
#11999=ORIENTED_EDGE ( 'NONE', *, *, #17102, .F. ) ;
#12005=CYLINDRICAL_SURFACE ( 'NONE', #22677, 5.460999999999938126 ) ;
#12009=DIRECTION ( 'NONE',  ( -2.330758767204999802E-14, -1.000000000000000000, -1.206582004152999850E-12 ) ) ;
#12015=CYLINDRICAL_SURFACE ( 'NONE', #4535, 3.175000000000149925 ) ;
#12057=LINE ( 'NONE', #19211, #4683 ) ;
#12080=ADVANCED_FACE ( 'NONE', ( #15233 ), #11824, .T. ) ;
#12133=AXIS2_PLACEMENT_3D ( 'NONE', #13910, #1363, #7009 ) ;
#12187=LINE ( 'NONE', #19103, #21092 ) ;
#12197=VERTEX_POINT ( 'NONE', #19329 ) ;
#12280=EDGE_CURVE ( 'NONE', #7536, #22551, #12057, .T. ) ;
#12281=CARTESIAN_POINT ( 'NONE',  ( -12.31900000000000084, -3660.140000000000327, 2247.392000000000280 ) ) ;
#12299=EDGE_CURVE ( 'NONE', #16784, #2492, #11047, .T. ) ;
#12372=ADVANCED_FACE ( 'NONE', ( #18257 ), #13098, .T. ) ;
#12409=VERTEX_POINT ( 'NONE', #10883 ) ;
#12454=LINE ( 'NONE', #6617, #20504 ) ;
#12486=ORIENTED_EDGE ( 'NONE', *, *, #17355, .F. ) ;
#12507=EDGE_CURVE ( 'NONE', #952, #10748, #18705, .T. ) ;
#12578=ORIENTED_EDGE ( 'NONE', *, *, #21463, .T. ) ;
#12643=ORIENTED_EDGE ( 'NONE', *, *, #13712, .T. ) ;
#12644=DIRECTION ( 'NONE',  ( -1.000000000000000000, 0.000000000000000000, 0.000000000000000000 ) ) ;
#12688=ADVANCED_FACE ( 'NONE', ( #6770 ), #1722, .T. ) ;
#12704=VECTOR ( 'NONE', #4867, 1000.000000000000000 ) ;
#12711=CIRCLE ( 'NONE', #15314, 5.460999999999938126 ) ;
#12786=PRODUCT_DEFINITION ( 'UNKNOWN', '', #10138, #11831 ) ;
#12799=FACE_OUTER_BOUND ( 'NONE', #598, .T. ) ;
#12801=EDGE_CURVE ( 'NONE', #10748, #16863, #7345, .T. ) ;
#12817=CARTESIAN_POINT ( 'NONE',  ( -12.69999999999999929, -3658.573829546965044, 2244.679313203020683 ) ) ;
#12818=ORIENTED_EDGE ( 'NONE', *, *, #13712, .F. ) ;
#12826=ORIENTED_EDGE ( 'NONE', *, *, #2844, .T. ) ;
#12833=DIRECTION ( 'NONE',  ( 1.000000000000000000, 0.000000000000000000, 0.000000000000000000 ) ) ;
#12853=CARTESIAN_POINT ( 'NONE',  ( -12.69999999979406091, -3657.265370510263438, 2247.391999999993459 ) ) ;
#12932=DIRECTION ( 'NONE',  ( 0.000000000000000000, -1.000000000000000000, 0.000000000000000000 ) ) ;
#12958=ORIENTED_EDGE ( 'NONE', *, *, #4770, .F. ) ;
#12977=DIRECTION ( 'NONE',  ( -1.744774614850039793E-12, -0.5000000000047110094, -0.8660254037817188832 ) ) ;
#13077=ORIENTED_EDGE ( 'NONE', *, *, #4779, .F. ) ;
#13098=PLANE ( 'NONE',  #10677 ) ;
#13144=AXIS2_PLACEMENT_3D ( 'NONE', #21377, #15515, #6857 ) ;
#13179=PLANE ( 'NONE',  #57 ) ;
#13187=DIRECTION ( 'NONE',  ( 2.339144844575037611E-14, 0.000000000000000000, 1.000000000000000000 ) ) ;
#13205=VERTEX_POINT ( 'NONE', #15642 ) ;
#13207=DIRECTION ( 'NONE',  ( 2.339144844575037611E-14, 0.000000000000000000, 1.000000000000000000 ) ) ;
#13209=DIRECTION ( 'NONE',  ( 1.000000000000000000, -2.334777064353000131E-14, -2.343004830739999973E-14 ) ) ;
#13279=DIRECTION ( 'NONE',  ( 2.330758767201999921E-14, 1.000000000000000000, -5.460979050843892707E-28 ) ) ;
#13290=EDGE_CURVE ( 'NONE', #6658, #15415, #15048, .T. ) ;
#13312=CARTESIAN_POINT ( 'NONE',  ( -12.31900000000000084, -3661.486200000000281, 2249.723686796999573 ) ) ;
#13375=CARTESIAN_POINT ( 'NONE',  ( -12.54218463261975813, -3662.832400000410871, 2247.392000000001190 ) ) ;
#13399=DIRECTION ( 'NONE',  ( -2.318894227180156550E-14, -1.000000000000000000, 0.000000000000000000 ) ) ;
#13440=DIRECTION ( 'NONE',  ( 3.212101257670982882E-14, 0.5000000000050977000, 0.8660254037814953954 ) ) ;
#13499=EDGE_CURVE ( 'NONE', #16275, #21968, #22642, .T. ) ;
#13560=MANIFOLD_SOLID_BREP ( 'TORNILLO4[1]', #3489 ) ;
#13597=CARTESIAN_POINT ( 'NONE',  ( -8.890000000022000748, -3661.486200000000281, 2245.060313203000078 ) ) ;
#13670=FACE_OUTER_BOUND ( 'NONE', #8377, .T. ) ;
#13687=EDGE_LOOP ( 'NONE', ( #1698, #19447, #17211, #20284, #17726, #4812 ) ) ;
#13702=ADVANCED_FACE ( 'NONE', ( #16414 ), #16071, .T. ) ;
#13712=EDGE_CURVE ( 'NONE', #8893, #2492, #15549, .T. ) ;
#13748=CARTESIAN_POINT ( 'NONE',  ( -12.69999999999999929, -3657.007659095000236, 2247.392000000000280 ) ) ;
#13864=DIRECTION ( 'NONE',  ( -1.000000000000000000, 0.000000000000000000, 1.295098308114000000E-13 ) ) ;
#13910=CARTESIAN_POINT ( 'NONE',  ( -8.890000000004999237, -3662.832400000000234, 2247.392000000000280 ) ) ;
#13911=DIRECTION ( 'NONE',  ( 2.330758767201999921E-14, 1.000000000000000000, 0.000000000000000000 ) ) ;
#14010=ORIENTED_EDGE ( 'NONE', *, *, #11854, .F. ) ;
#14050=AXIS2_PLACEMENT_3D ( 'NONE', #4139, #18431, #20312 ) ;
#14129=DIRECTION ( 'NONE',  ( -1.000000000000000000, 0.000000000000000000, 0.000000000000000000 ) ) ;
#14154=DIRECTION ( 'NONE',  ( -1.000000000000000000, 2.330758767201999921E-14, 2.343004830739999973E-14 ) ) ;
#14232=DIRECTION ( 'NONE',  ( -2.334777064352623371E-14, -1.000000000000000000, 0.000000000000000000 ) ) ;
#14260=EDGE_CURVE ( 'NONE', #6431, #12197, #17702, .T. ) ;
#14317=CARTESIAN_POINT ( 'NONE',  ( -12.31900000000000084, -3662.489255679000053, 2248.748343399000532 ) ) ;
#14337=ORIENTED_EDGE ( 'NONE', *, *, #15846, .T. ) ;
#14392=EDGE_CURVE ( 'NONE', #22551, #20085, #21951, .T. ) ;
#14425=ORIENTED_EDGE ( 'NONE', *, *, #15609, .T. ) ;
#14427=ADVANCED_FACE ( 'NONE', ( #19624 ), #20691, .T. ) ;
#14473=CIRCLE ( 'NONE', #18955, 0.3809999999999993947 ) ;
#14541=DIRECTION ( 'NONE',  ( 5.154430176750962410E-12, -0.5000000000031962211, 0.8660254037825932949 ) ) ;
#14542=CARTESIAN_POINT ( 'NONE',  ( -12.31900000000000084, -3658.793800000000374, 2245.060313203000078 ) ) ;
#14613=CARTESIAN_POINT ( 'NONE',  ( -8.890000000032001637, -3658.793800000000374, 2245.060313203000078 ) ) ;
#14624=CARTESIAN_POINT ( 'NONE',  ( -12.31900000000000084, -3660.140000000000327, 2247.392000000000280 ) ) ;
#14681=DIRECTION ( 'NONE',  ( 0.000000000000000000, 2.331176954593720496E-12, -1.000000000000000000 ) ) ;
#14699=CYLINDRICAL_SURFACE ( 'NONE', #20091, 0.3810000000000151599 ) ;
#14712=LINE ( 'NONE', #15800, #5760 ) ;
#14756=DIRECTION ( 'NONE',  ( 2.330758767201999921E-14, 1.000000000000000000, 0.000000000000000000 ) ) ;
#14795=CARTESIAN_POINT ( 'NONE',  ( -12.31900000000002393, -3661.486200000138069, 2245.060313203176065 ) ) ;
#14818=AXIS2_PLACEMENT_3D ( 'NONE', #1719, #22909, #8631 ) ;
#14885=EDGE_CURVE ( 'NONE', #19933, #3991, #12187, .T. ) ;
#14904=VECTOR ( 'NONE', #18240, 1000.000000000000114 ) ;
#15018=ORIENTED_EDGE ( 'NONE', *, *, #7848, .T. ) ;
#15033=VERTEX_POINT ( 'NONE', #6318 ) ;
#15040=AXIS2_PLACEMENT_3D ( 'NONE', #3999, #16304, #2242 ) ;
#15048=( BOUNDED_CURVE ( )  B_SPLINE_CURVE ( 3, ( #12817, #289, #18088, #3909 ),
 .UNSPECIFIED., .F., .T. ) 
 B_SPLINE_CURVE_WITH_KNOTS ( ( 4, 4 ),
 ( 1.570796326836454426, 3.141592653589801110 ),
 .UNSPECIFIED. ) 
 CURVE ( )  GEOMETRIC_REPRESENTATION_ITEM ( )  RATIONAL_B_SPLINE_CURVE ( ( 1.000000000000000000, 0.8047378541341584368, 0.8047378541341584368, 1.000000000000000000 ) ) 
 REPRESENTATION_ITEM ( '' )  );
#15066=DIRECTION ( 'NONE',  ( 1.000000000000000000, -2.334777064353000131E-14, -2.343004830739999973E-14 ) ) ;
#15133=ADVANCED_FACE ( 'NONE', ( #2447 ), #817, .T. ) ;
#15156=PRODUCT_CONTEXT ( 'NONE', #4076, 'mechanical' ) ;
#15206=CARTESIAN_POINT ( 'NONE',  ( -8.890000000008999592, -3662.832400000000234, 2247.392000000000280 ) ) ;
#15207=LINE ( 'NONE', #22336, #3577 ) ;
#15212=ORIENTED_EDGE ( 'NONE', *, *, #18020, .F. ) ;
#15233=FACE_OUTER_BOUND ( 'NONE', #3804, .T. ) ;
#15296=EDGE_CURVE ( 'NONE', #2826, #16505, #20307, .T. ) ;
#15304=FACE_OUTER_BOUND ( 'NONE', #7748, .T. ) ;
#15309=DIRECTION ( 'NONE',  ( -1.000000000000000000, 0.000000000000000000, 0.000000000000000000 ) ) ;
#15314=AXIS2_PLACEMENT_3D ( 'NONE', #538, #15066, #2193 ) ;
#15328=CARTESIAN_POINT ( 'NONE',  ( 19.05000000000000071, -3660.140000000000327, 2247.392000000000280 ) ) ;
#15360=EDGE_CURVE ( 'NONE', #20085, #19933, #1276, .T. ) ;
#15365=EDGE_CURVE ( 'NONE', #1958, #7536, #16680, .T. ) ;
#15383=SHAPE_DEFINITION_REPRESENTATION ( #3002, #15665 ) ;
#15395=ORIENTED_EDGE ( 'NONE', *, *, #4070, .F. ) ;
#15415=VERTEX_POINT ( 'NONE', #16480 ) ;
#15463=VERTEX_POINT ( 'NONE', #22091 ) ;
#15477=DIRECTION ( 'NONE',  ( -2.159861190483010203E-14, 0.5000000000030029312, -0.8660254037827048723 ) ) ;
#15495=LINE ( 'NONE', #13748, #15941 ) ;
#15507=VECTOR ( 'NONE', #7400, 1000.000000000000000 ) ;
#15515=DIRECTION ( 'NONE',  ( -1.000000000000000000, 2.330758767201999921E-14, 2.343004830739999973E-14 ) ) ;
#15549=CIRCLE ( 'NONE', #21905, 1.904999999999823501 ) ;
#15557=VERTEX_POINT ( 'NONE', #18690 ) ;
#15560=CIRCLE ( 'NONE', #8458, 5.079999999999973426 ) ;
#15609=EDGE_CURVE ( 'NONE', #16863, #15557, #6062, .T. ) ;
#15634=CARTESIAN_POINT ( 'NONE',  ( -8.890000000028999594, -3656.101400000000012, 2245.060313203000078 ) ) ;
#15636=ORIENTED_EDGE ( 'NONE', *, *, #22391, .T. ) ;
#15642=CARTESIAN_POINT ( 'NONE',  ( -8.890000000026999416, -3657.447599999999966, 2247.392000000000280 ) ) ;
#15665=SHAPE_REPRESENTATION ( 'Screw 2', ( #5611 ), #2257 ) ;
#15720=ADVANCED_FACE ( 'NONE', ( #15304 ), #12015, .T. ) ;
#15773=VECTOR ( 'NONE', #11431, 1000.000000000000000 ) ;
#15800=CARTESIAN_POINT ( 'NONE',  ( 19.05000000000000071, -3663.315000000000509, 2247.392000000000280 ) ) ;
#15846=EDGE_CURVE ( 'NONE', #22551, #3991, #20716, .T. ) ;
#15926=DIRECTION ( 'NONE',  ( 0.000000000000000000, 0.8660254037820785955, -0.5000000000040877302 ) ) ;
#15941=VECTOR ( 'NONE', #10452, 1000.000000000000114 ) ;
#15964=CARTESIAN_POINT ( 'NONE',  ( 20.32000000000000028, -3658.235000000000127, 2247.392000000000280 ) ) ;
#16017=CARTESIAN_POINT ( 'NONE',  ( -12.69999999999999929, -3660.140000000000327, 2247.392000000000280 ) ) ;
#16071=CYLINDRICAL_SURFACE ( 'NONE', #9911, 3.175000000000149925 ) ;
#16132=CARTESIAN_POINT ( 'NONE',  ( -12.69999999999999929, -3658.573829547000059, 2244.679313203000220 ) ) ;
#16136=ORIENTED_EDGE ( 'NONE', *, *, #17310, .T. ) ;
#16163=CARTESIAN_POINT ( 'NONE',  ( -6.349999999999999645, -3660.140000000000327, 2247.392000000000280 ) ) ;
#16226=VERTEX_POINT ( 'NONE', #21480 ) ;
#16275=VERTEX_POINT ( 'NONE', #9405 ) ;
#16304=DIRECTION ( 'NONE',  ( 0.000000000000000000, -0.8660254037840939834, -0.5000000000005969669 ) ) ;
#16321=CARTESIAN_POINT ( 'NONE',  ( -6.349999999999999645, -3654.679000000000087, 2247.392000000000280 ) ) ;
#16326=AXIS2_PLACEMENT_3D ( 'NONE', #20567, #15309, #2996 ) ;
#16340=DIRECTION ( 'NONE',  ( -1.000000000000000000, 0.000000000000000000, 0.000000000000000000 ) ) ;
#16349=FACE_OUTER_BOUND ( 'NONE', #17958, .T. ) ;
#16414=FACE_OUTER_BOUND ( 'NONE', #11196, .T. ) ;
#16451=EDGE_LOOP ( 'NONE', ( #16895, #3931, #6562, #15636, #8394 ) ) ;
#16456=DIRECTION ( 'NONE',  ( -1.000000000000000000, 2.330758767201999921E-14, 2.356218894535000080E-14 ) ) ;
#16480=CARTESIAN_POINT ( 'NONE',  ( -12.31900000000000084, -3658.793799999878502, 2245.060313203211081 ) ) ;
#16483=CARTESIAN_POINT ( 'NONE',  ( -8.890000000017000303, -3658.793800000000374, 2249.723686796999573 ) ) ;
#16505=VERTEX_POINT ( 'NONE', #4784 ) ;
#16600=CARTESIAN_POINT ( 'NONE',  ( 20.32000000000000028, -3660.140000000000327, 2247.392000000000280 ) ) ;
#16657=CARTESIAN_POINT ( 'NONE',  ( -12.69999999985358308, -3663.014629489800427, 2247.392000000001190 ) ) ;
#16680=( BOUNDED_CURVE ( )  B_SPLINE_CURVE ( 3, ( #322, #12853, #18239, #5722 ),
 .UNSPECIFIED., .F., .F. ) 
 B_SPLINE_CURVE_WITH_KNOTS ( ( 4, 4 ),
 ( 1.570796327717542518, 3.141592653589902806 ),
 .UNSPECIFIED. ) 
 CURVE ( )  GEOMETRIC_REPRESENTATION_ITEM ( )  RATIONAL_B_SPLINE_CURVE ( ( 1.000000000000000000, 0.8047378543418087782, 0.8047378543418087782, 1.000000000000000000 ) ) 
 REPRESENTATION_ITEM ( '' )  );
#16722=EDGE_LOOP ( 'NONE', ( #6831, #9517, #5380, #5817, #4499 ) ) ;
#16741=UNCERTAINTY_MEASURE_WITH_UNIT (LENGTH_MEASURE( 1.000000000000000082E-05 ), #21126, 'distance_accuracy_value', 'NONE');
#16742=EDGE_LOOP ( 'NONE', ( #5106, #9592, #4182, #7973, #15212 ) ) ;
#16784=VERTEX_POINT ( 'NONE', #2641 ) ;
#16797=CARTESIAN_POINT ( 'NONE',  ( -12.69999999999999929, -3658.573829546965044, 2244.679313203020683 ) ) ;
#16806=CARTESIAN_POINT ( 'NONE',  ( -8.890000000047999507, -3658.793800000000374, 2245.060313203000078 ) ) ;
#16812=DIRECTION ( 'NONE',  ( -1.000000000000000000, 0.000000000000000000, -1.295098308109999907E-13 ) ) ;
#16832=DIRECTION ( 'NONE',  ( -1.000000000000000000, 3.885294924331999768E-13, 2.590196616220999964E-13 ) ) ;
#16863=VERTEX_POINT ( 'NONE', #10727 ) ;
#16867=CARTESIAN_POINT ( 'NONE',  ( 19.05000000000000071, -3662.045000000000073, 2247.392000000000280 ) ) ;
#16895=ORIENTED_EDGE ( 'NONE', *, *, #21406, .F. ) ;
#16941=ORIENTED_EDGE ( 'NONE', *, *, #20590, .T. ) ;
#16944=DIRECTION ( 'NONE',  ( -1.000000000000000000, 2.330758767201999921E-14, 2.343004830739999973E-14 ) ) ;
#16973=DIRECTION ( 'NONE',  ( -2.330758767202000237E-14, -1.000000000000000000, -1.224646799141892318E-16 ) ) ;
#16979=EDGE_LOOP ( 'NONE', ( #4853, #14337, #7191, #1179 ) ) ;
#16981=DIRECTION ( 'NONE',  ( -0.000000000000000000, 1.224646799147353207E-16, 1.000000000000000000 ) ) ;
#17102=EDGE_CURVE ( 'NONE', #20980, #7476, #7972, .T. ) ;
#17141=DIRECTION ( 'NONE',  ( -1.000000000000000000, 0.000000000000000000, 0.000000000000000000 ) ) ;
#17163=EDGE_CURVE ( 'NONE', #16275, #16505, #9176, .T. ) ;
#17211=ORIENTED_EDGE ( 'NONE', *, *, #15296, .F. ) ;
#17233=CARTESIAN_POINT ( 'NONE',  ( 19.05000000000000071, -3663.315000000000509, 2247.392000000000280 ) ) ;
#17310=EDGE_CURVE ( 'NONE', #10748, #2928, #8484, .T. ) ;
#17335=CARTESIAN_POINT ( 'NONE',  ( -12.69999999999998153, -3658.573829547082369, 2250.104686796773422 ) ) ;
#17337=AXIS2_PLACEMENT_3D ( 'NONE', #5694, #16456, #411 ) ;
#17355=EDGE_CURVE ( 'NONE', #7476, #15463, #11323, .T. ) ;
#17356=CARTESIAN_POINT ( 'NONE',  ( -8.890000000017000303, -3658.793800000000374, 2249.723686796999573 ) ) ;
#17365=DIRECTION ( 'NONE',  ( -4.457711412217000029E-12, 1.000000000000000000, 0.000000000000000000 ) ) ;
#17374=EDGE_LOOP ( 'NONE', ( #20519, #1326 ) ) ;
#17405=AXIS2_PLACEMENT_3D ( 'NONE', #20961, #15926, #3145 ) ;
#17408=CIRCLE ( 'NONE', #6963, 3.175000000000149925 ) ;
#17565=DIRECTION ( 'NONE',  ( 1.163002179513000119E-14, 1.000000000000000000, 9.924285265180999807E-13 ) ) ;
#17702=CIRCLE ( 'NONE', #18818, 3.175000000000149925 ) ;
#17726=ORIENTED_EDGE ( 'NONE', *, *, #7848, .F. ) ;
#17730=AXIS2_PLACEMENT_3D ( 'NONE', #19625, #22891, #3567 ) ;
#17743=DIRECTION ( 'NONE',  ( -1.000000000000000000, 0.000000000000000000, 0.000000000000000000 ) ) ;
#17948=ADVANCED_FACE ( 'NONE', ( #16349 ), #4255, .T. ) ;
#17958=EDGE_LOOP ( 'NONE', ( #1031, #20365, #19198, #12818 ) ) ;
#17976=DIRECTION ( 'NONE',  ( 0.000000000000000000, 0.8660254037838039931, 0.5000000000010993428 ) ) ;
#17985=EDGE_CURVE ( 'NONE', #21023, #6431, #14712, .T. ) ;
#17997=AXIS2_PLACEMENT_3D ( 'NONE', #11637, #4397, #2523 ) ;
#18012=CARTESIAN_POINT ( 'NONE',  ( -12.54218463272304085, -3661.486200000483223, 2249.723686796998663 ) ) ;
#18020=EDGE_CURVE ( 'NONE', #15463, #7476, #6138, .T. ) ;
#18088=CARTESIAN_POINT ( 'NONE',  ( -12.54218463272850137, -3658.793799999516068, 2245.060313203004171 ) ) ;
#18200=FACE_OUTER_BOUND ( 'NONE', #1935, .T. ) ;
#18239=CARTESIAN_POINT ( 'NONE',  ( -12.54218463257254612, -3657.447599999590238, 2247.391999999993914 ) ) ;
#18240=DIRECTION ( 'NONE',  ( -3.591349225554024811E-12, 0.5000000000004030110, -0.8660254037842058938 ) ) ;
#18257=FACE_OUTER_BOUND ( 'NONE', #18687, .T. ) ;
#18302=CARTESIAN_POINT ( 'NONE',  ( -12.54218463262903605, -3661.486200000482768, 2245.060313202995985 ) ) ;
#18313=DIRECTION ( 'NONE',  ( 0.000000000000000000, 0.8660254037817070039, -0.5000000000047313264 ) ) ;
#18378=CIRCLE ( 'NONE', #17997, 0.3810000000000002829 ) ;
#18399=ORIENTED_EDGE ( 'NONE', *, *, #22579, .F. ) ;
#18413=AXIS2_PLACEMENT_3D ( 'NONE', #4110, #9836, #6338 ) ;
#18431=DIRECTION ( 'NONE',  ( 1.000000000000000000, -2.334777064353000131E-14, -2.343004830739999973E-14 ) ) ;
#18437=VECTOR ( 'NONE', #7302, 1000.000000000000000 ) ;
#18444=DIRECTION ( 'NONE',  ( -1.000000000000000000, 0.000000000000000000, 0.000000000000000000 ) ) ;
#18493=ORIENTED_EDGE ( 'NONE', *, *, #14392, .T. ) ;
#18515=FACE_OUTER_BOUND ( 'NONE', #16722, .T. ) ;
#18519=AXIS2_PLACEMENT_3D ( 'NONE', #18980, #18627, #6218 ) ;
#18536=VECTOR ( 'NONE', #16832, 1000.000000000000000 ) ;
#18603=DIRECTION ( 'NONE',  ( -2.334777064352623371E-14, -1.000000000000000000, 0.000000000000000000 ) ) ;
#18627=DIRECTION ( 'NONE',  ( 0.000000000000000000, 0.5000000000031962211, -0.8660254037825932949 ) ) ;
#18645=CARTESIAN_POINT ( 'NONE',  ( -12.31899999999998663, -3662.832400000169400, 2247.392000000001190 ) ) ;
#18687=EDGE_LOOP ( 'NONE', ( #3412, #7714, #5881, #19113 ) ) ;
#18690=CARTESIAN_POINT ( 'NONE',  ( -8.890000000022000748, -3661.486200000000281, 2245.060313203000078 ) ) ;
#18705=LINE ( 'NONE', #15206, #18536 ) ;
#18726=ORIENTED_EDGE ( 'NONE', *, *, #21406, .T. ) ;
#18781=LINE ( 'NONE', #20539, #8536 ) ;
#18818=AXIS2_PLACEMENT_3D ( 'NONE', #3448, #17743, #10366 ) ;
#18942=CIRCLE ( 'NONE', #16326, 3.175000000000149925 ) ;
#18955=AXIS2_PLACEMENT_3D ( 'NONE', #2463, #16973, #11819 ) ;
#18980=CARTESIAN_POINT ( 'NONE',  ( -12.31900000000000084, -3662.489255679000053, 2246.035656601000028 ) ) ;
#18987=LINE ( 'NONE', #13597, #296 ) ;
#19002=EDGE_LOOP ( 'NONE', ( #14010, #14425, #12826, #2796 ) ) ;
#19035=DIRECTION ( 'NONE',  ( -1.000000000000000000, 0.000000000000000000, 0.000000000000000000 ) ) ;
#19086=CARTESIAN_POINT ( 'NONE',  ( -6.731000000000127770, -3660.140000000000327, 2241.931000000000040 ) ) ;
#19103=CARTESIAN_POINT ( 'NONE',  ( -12.69999999999999929, -3661.706170452999686, 2250.104686796999886 ) ) ;
#19113=ORIENTED_EDGE ( 'NONE', *, *, #22759, .T. ) ;
#19161=LINE ( 'NONE', #3217, #19246 ) ;
#19198=ORIENTED_EDGE ( 'NONE', *, *, #12299, .T. ) ;
#19208=FACE_OUTER_BOUND ( 'NONE', #4524, .T. ) ;
#19211=CARTESIAN_POINT ( 'NONE',  ( -12.31900000000000084, -3657.447599999999966, 2247.392000000000280 ) ) ;
#19246=VECTOR ( 'NONE', #517, 1000.000000000000000 ) ;
#19323=CARTESIAN_POINT ( 'NONE',  ( 19.05000000000000071, -3660.140000000000327, 2247.392000000000280 ) ) ;
#19329=CARTESIAN_POINT ( 'NONE',  ( -6.349999999999999645, -3656.965000000000146, 2247.392000000000280 ) ) ;
#19379=ORIENTED_EDGE ( 'NONE', *, *, #8158, .F. ) ;
#19380=ORIENTED_EDGE ( 'NONE', *, *, #6161, .F. ) ;
#19447=ORIENTED_EDGE ( 'NONE', *, *, #17163, .T. ) ;
#19505=FACE_OUTER_BOUND ( 'NONE', #20517, .T. ) ;
#19537=CIRCLE ( 'NONE', #451, 1.269999999999882334 ) ;
#19624=FACE_OUTER_BOUND ( 'NONE', #20998, .T. ) ;
#19625=CARTESIAN_POINT ( 'NONE',  ( -8.890000000036000216, -3661.486200000000281, 2245.060313203000078 ) ) ;
#19699=CIRCLE ( 'NONE', #8837, 0.3810000000000002829 ) ;
#19738=ORIENTED_EDGE ( 'NONE', *, *, #17163, .F. ) ;
#19788=ORIENTED_EDGE ( 'NONE', *, *, #17985, .F. ) ;
#19933=VERTEX_POINT ( 'NONE', #10296 ) ;
#19956=CARTESIAN_POINT ( 'NONE',  ( -12.70000000000007923, -3661.706170452909191, 2244.679313203225774 ) ) ;
#19984=CARTESIAN_POINT ( 'NONE',  ( -12.54218463262979988, -3658.793799999511066, 2249.723686797001392 ) ) ;
#20061=PLANE ( 'NONE',  #15040 ) ;
#20075=DIRECTION ( 'NONE',  ( 2.330758767208999958E-14, 1.000000000000000000, 2.848874176402999842E-12 ) ) ;
#20085=VERTEX_POINT ( 'NONE', #4527 ) ;
#20091=AXIS2_PLACEMENT_3D ( 'NONE', #10717, #21502, #17976 ) ;
#20096=AXIS2_PLACEMENT_3D ( 'NONE', #15634, #21368, #17365 ) ;
#20129=LINE ( 'NONE', #16483, #14904 ) ;
#20167=EDGE_CURVE ( 'NONE', #952, #16226, #676, .T. ) ;
#20200=ORIENTED_EDGE ( 'NONE', *, *, #1102, .F. ) ;
#20266=EDGE_CURVE ( 'NONE', #16784, #21023, #8086, .T. ) ;
#20284=ORIENTED_EDGE ( 'NONE', *, *, #214, .F. ) ;
#20307=CIRCLE ( 'NONE', #21426, 5.460999999999938126 ) ;
#20312=DIRECTION ( 'NONE',  ( -2.334777064352623371E-14, -1.000000000000000000, 0.000000000000000000 ) ) ;
#20346=ORIENTED_EDGE ( 'NONE', *, *, #15846, .F. ) ;
#20348=CARTESIAN_POINT ( 'NONE',  ( -12.31900000000000084, -3661.486200000000281, 2245.060313203000078 ) ) ;
#20365=ORIENTED_EDGE ( 'NONE', *, *, #6945, .T. ) ;
#20467=ORIENTED_EDGE ( 'NONE', *, *, #13290, .F. ) ;
#20504=VECTOR ( 'NONE', #13864, 1000.000000000000000 ) ;
#20516=CARTESIAN_POINT ( 'NONE',  ( -12.70000000000005080, -3663.272340905245528, 2247.392000000001644 ) ) ;
#20517=EDGE_LOOP ( 'NONE', ( #19738, #7950, #11715, #15018, #9697, #8575 ) ) ;
#20519=ORIENTED_EDGE ( 'NONE', *, *, #14260, .T. ) ;
#20520=CIRCLE ( 'NONE', #22028, 5.460999999999938126 ) ;
#20539=CARTESIAN_POINT ( 'NONE',  ( 19.05000000000000071, -3656.965000000000146, 2247.392000000000280 ) ) ;
#20542=ORIENTED_EDGE ( 'NONE', *, *, #7949, .T. ) ;
#20558=ORIENTED_EDGE ( 'NONE', *, *, #22759, .F. ) ;
#20567=CARTESIAN_POINT ( 'NONE',  ( -6.349999999999999645, -3660.140000000000327, 2247.392000000000280 ) ) ;
#20590=EDGE_CURVE ( 'NONE', #13205, #7536, #8601, .T. ) ;
#20675=ORIENTED_EDGE ( 'NONE', *, *, #13290, .T. ) ;
#20680=DIRECTION ( 'NONE',  ( -1.000000000000000000, 0.000000000000000000, 0.000000000000000000 ) ) ;
#20691=TOROIDAL_SURFACE ( 'NONE', #9121, 5.080000000000000071, 0.3810000000000000053 ) ;
#20716=( BOUNDED_CURVE ( )  B_SPLINE_CURVE ( 3, ( #8968, #19984, #3917, #7100 ),
 .UNSPECIFIED., .F., .T. ) 
 B_SPLINE_CURVE_WITH_KNOTS ( ( 4, 4 ),
 ( 4.051959034059917173E-16, 1.570796326195641912 ),
 .UNSPECIFIED. ) 
 CURVE ( )  GEOMETRIC_REPRESENTATION_ITEM ( )  RATIONAL_B_SPLINE_CURVE ( ( 1.000000000000000000, 0.8047378542656107303, 0.8047378542656107303, 1.000000000000000000 ) ) 
 REPRESENTATION_ITEM ( '' )  );
#20718=CIRCLE ( 'NONE', #9809, 5.079999999999973426 ) ;
#20763=CARTESIAN_POINT ( 'NONE',  ( -12.69999999999999929, -3661.706170452999686, 2250.104686796999886 ) ) ;
#20785=ORIENTED_EDGE ( 'NONE', *, *, #4770, .T. ) ;
#20814=ADVANCED_FACE ( 'NONE', ( #18200 ), #9065, .T. ) ;
#20820=PLANE ( 'NONE',  #545 ) ;
#20916=FACE_OUTER_BOUND ( 'NONE', #13687, .T. ) ;
#20928=LINE ( 'NONE', #2642, #12704 ) ;
#20951=AXIS2_PLACEMENT_3D ( 'NONE', #9193, #16340, #294 ) ;
#20961=CARTESIAN_POINT ( 'NONE',  ( -8.890000000006001102, -3661.486200000000281, 2249.723686796999573 ) ) ;
#20980=VERTEX_POINT ( 'NONE', #6362 ) ;
#20983=AXIS2_PLACEMENT_3D ( 'NONE', #16600, #5844, #2426 ) ;
#20998=EDGE_LOOP ( 'NONE', ( #6135, #11343, #9550, #12486, #11999 ) ) ;
#21023=VERTEX_POINT ( 'NONE', #17233 ) ;
#21092=VECTOR ( 'NONE', #17565, 1000.000000000000000 ) ;
#21126=( LENGTH_UNIT ( ) NAMED_UNIT ( * ) SI_UNIT ( .MILLI., .METRE. ) );
#21140=AXIS2_PLACEMENT_3D ( 'NONE', #14317, #21458, #5410 ) ;
#21148=ORIENTED_EDGE ( 'NONE', *, *, #1102, .T. ) ;
#21176=PRODUCT ( 'Screw 2', 'Screw 2', '', ( #15156 ) ) ;
#21275=DIRECTION ( 'NONE',  ( 2.330758767201999921E-14, 1.000000000000000000, -5.460979050843892707E-28 ) ) ;
#21280=AXIS2_PLACEMENT_3D ( 'NONE', #9053, #20075, #14681 ) ;
#21281=EDGE_LOOP ( 'NONE', ( #2637, #1898, #10541, #1136 ) ) ;
#21368=DIRECTION ( 'NONE',  ( 1.000000000000000000, 4.457711412217000029E-12, 2.901972884401000201E-13 ) ) ;
#21374=CARTESIAN_POINT ( 'NONE',  ( -12.31900000000000084, -3657.790744320999693, 2246.035656601000028 ) ) ;
#21377=CARTESIAN_POINT ( 'NONE',  ( -6.730999999999999872, -3660.140000000000327, 2247.392000000000280 ) ) ;
#21406=EDGE_CURVE ( 'NONE', #12409, #22852, #15560, .T. ) ;
#21426=AXIS2_PLACEMENT_3D ( 'NONE', #12281, #23042, #10515 ) ;
#21458=DIRECTION ( 'NONE',  ( -3.194481088215918719E-14, -0.5000000000040877302, -0.8660254037820785955 ) ) ;
#21463=EDGE_CURVE ( 'NONE', #6658, #1958, #15207, .T. ) ;
#21480=CARTESIAN_POINT ( 'NONE',  ( -8.890000000008001280, -3661.486200000000281, 2249.723686796999573 ) ) ;
#21502=DIRECTION ( 'NONE',  ( 0.000000000000000000, -0.5000000000005969669, 0.8660254037840939834 ) ) ;
#21504=DIRECTION ( 'NONE',  ( -2.343004830739999973E-14, -1.784212334590129905E-30, -1.000000000000000000 ) ) ;
#21514=ORIENTED_EDGE ( 'NONE', *, *, #4955, .F. ) ;
#21519=DIRECTION ( 'NONE',  ( 0.000000000000000000, 0.000000000000000000, 1.000000000000000000 ) ) ;
#21524=CARTESIAN_POINT ( 'NONE',  ( -12.31900000000000084, -3662.832400000000234, 2247.392000000000280 ) ) ;
#21601=VECTOR ( 'NONE', #1997, 1000.000000000000114 ) ;
#21605=ADVANCED_FACE ( 'NONE', ( #1365, #8528 ), #7010, .T. ) ;
#21623=CARTESIAN_POINT ( 'NONE',  ( -12.31900000000000084, -3658.793800000000374, 2249.723686796999573 ) ) ;
#21666=DIRECTION ( 'NONE',  ( 0.000000000000000000, 0.000000000000000000, -1.000000000000000000 ) ) ;
#21729=CARTESIAN_POINT ( 'NONE',  ( -6.349999999999999645, -3660.140000000000327, 2247.392000000000280 ) ) ;
#21739=DIRECTION ( 'NONE',  ( -1.000000000000000000, 0.000000000000000000, 0.000000000000000000 ) ) ;
#21761=CARTESIAN_POINT ( 'NONE',  ( -12.31900000000000084, -3661.486200000121244, 2249.723686796789480 ) ) ;
#21806=ORIENTED_EDGE ( 'NONE', *, *, #9438, .T. ) ;
#21843=CARTESIAN_POINT ( 'NONE',  ( -12.31899999999998663, -3662.832400000169400, 2247.392000000001190 ) ) ;
#21870=DIRECTION ( 'NONE',  ( -1.000000000000000000, 0.000000000000000000, 0.000000000000000000 ) ) ;
#21893=DIRECTION ( 'NONE',  ( -1.000000000000000000, 2.330758767201999921E-14, 2.343004830739999973E-14 ) ) ;
#21905=AXIS2_PLACEMENT_3D ( 'NONE', #7511, #11027, #5542 ) ;
#21935=CARTESIAN_POINT ( 'NONE',  ( -12.69999999999999929, -3660.140000000000327, 2247.392000000000280 ) ) ;
#21951=LINE ( 'NONE', #21623, #4979 ) ;
#21968=VERTEX_POINT ( 'NONE', #3444 ) ;
#21977=CARTESIAN_POINT ( 'NONE',  ( -6.350000000000118661, -3660.140000000000327, 2242.311999999999898 ) ) ;
#22028=AXIS2_PLACEMENT_3D ( 'NONE', #6081, #13209, #18603 ) ;
#22031=DIRECTION ( 'NONE',  ( -3.370353031811000117E-12, 1.000000000000000000, 1.649417656553999895E-12 ) ) ;
#22091=CARTESIAN_POINT ( 'NONE',  ( -12.69999999999988027, -3660.140000000000327, 2252.472000000000207 ) ) ;
#22102=ORIENTED_EDGE ( 'NONE', *, *, #10063, .F. ) ;
#22244=ADVANCED_FACE ( 'NONE', ( #9015, #5389 ), #7144, .F. ) ;
#22267=CARTESIAN_POINT ( 'NONE',  ( 19.05000000000000071, -3660.140000000000327, 2247.392000000000280 ) ) ;
#22268=CIRCLE ( 'NONE', #7329, 5.460999999999938126 ) ;
#22332=CARTESIAN_POINT ( 'NONE',  ( -12.31900000000000084, -3660.140000000000327, 2247.392000000000280 ) ) ;
#22333=CARTESIAN_POINT ( 'NONE',  ( -8.890000000008999592, -3662.832400000000234, 2247.392000000000280 ) ) ;
#22336=CARTESIAN_POINT ( 'NONE',  ( -12.69999999999999929, -3658.573829547000059, 2244.679313203000220 ) ) ;
#22340=CARTESIAN_POINT ( 'NONE',  ( -12.69999999999997442, -3657.007659094873816, 2247.391999999781547 ) ) ;
#22391=EDGE_CURVE ( 'NONE', #8227, #11037, #20520, .T. ) ;
#22412=VECTOR ( 'NONE', #6176, 1000.000000000000000 ) ;
#22443=DIRECTION ( 'NONE',  ( 2.216404975962025766E-13, 0.5000000000042060799, 0.8660254037820102058 ) ) ;
#22530=FACE_OUTER_BOUND ( 'NONE', #772, .T. ) ;
#22551=VERTEX_POINT ( 'NONE', #2075 ) ;
#22556=VERTEX_POINT ( 'NONE', #14613 ) ;
#22579=EDGE_CURVE ( 'NONE', #6658, #15033, #10506, .T. ) ;
#22642=CIRCLE ( 'NONE', #14050, 5.460999999999938126 ) ;
#22649=CARTESIAN_POINT ( 'NONE',  ( -8.890000000026999416, -3657.447599999999966, 2247.392000000000280 ) ) ;
#22652=CARTESIAN_POINT ( 'NONE',  ( -6.730999999999999872, -3660.140000000000327, 2247.392000000000280 ) ) ;
#22677=AXIS2_PLACEMENT_3D ( 'NONE', #21729, #7320, #12932 ) ;
#22759=EDGE_CURVE ( 'NONE', #16226, #20085, #11423, .T. ) ;
#22777=FACE_OUTER_BOUND ( 'NONE', #19002, .T. ) ;
#22807=ORIENTED_EDGE ( 'NONE', *, *, #20167, .T. ) ;
#22821=DIRECTION ( 'NONE',  ( -1.000000000000000000, 2.318894227180000040E-14, 2.343004830739999973E-14 ) ) ;
#22824=EDGE_CURVE ( 'NONE', #21968, #8227, #12711, .T. ) ;
#22852=VERTEX_POINT ( 'NONE', #21977 ) ;
#22891=DIRECTION ( 'NONE',  ( 0.000000000000000000, -2.848874176402999842E-12, 1.000000000000000000 ) ) ;
#22909=DIRECTION ( 'NONE',  ( 1.000000000000000000, 0.000000000000000000, 0.000000000000000000 ) ) ;
#22962=ORIENTED_EDGE ( 'NONE', *, *, #15360, .F. ) ;
#22998=ORIENTED_EDGE ( 'NONE', *, *, #5271, .T. ) ;
#23042=DIRECTION ( 'NONE',  ( -1.000000000000000000, 2.318894227180000040E-14, 2.343004830739999973E-14 ) ) ;
#23094=( NAMED_UNIT ( * ) SI_UNIT ( $, .STERADIAN. ) SOLID_ANGLE_UNIT ( ) );
#23108=( BOUNDED_CURVE ( )  B_SPLINE_CURVE ( 3, ( #19956, #11163, #18302, #14795 ),
 .UNSPECIFIED., .F., .T. ) 
 B_SPLINE_CURVE_WITH_KNOTS ( ( 4, 4 ),
 ( 1.570796327398617187, 3.141592653589748263 ),
 .UNSPECIFIED. ) 
 CURVE ( )  GEOMETRIC_REPRESENTATION_ITEM ( )  RATIONAL_B_SPLINE_CURVE ( ( 1.000000000000000000, 0.8047378542666738799, 0.8047378542666738799, 1.000000000000000000 ) ) 
 REPRESENTATION_ITEM ( '' )  );
#23130=ADVANCED_FACE ( 'NONE', ( #19505 ), #5103, .T. ) ;
#23157=VECTOR ( 'NONE', #1725, 1000.000000000000000 ) ;
#23208=COLOUR_RGB('Black',0.12,0.14,0.17);
#23209=FILL_AREA_STYLE_COLOUR('',#23208);
#23210=FILL_AREA_STYLE('',(#23209));
#23211=SURFACE_STYLE_FILL_AREA(#23210);
#23212=SURFACE_SIDE_STYLE('',(#23211));
#23213=SURFACE_STYLE_USAGE(.BOTH.,#23212);
#23214=PRESENTATION_STYLE_ASSIGNMENT((#23213));
#23227=STYLED_ITEM('',(#23214),#13560);
#23237=MECHANICAL_DESIGN_GEOMETRIC_PRESENTATION_REPRESENTATION('',(#23227),#2257);
ENDSEC;
END-ISO-10303-21;
